ISO-10303-21;
HEADER;
/* Generated by software containing ST-Developer
 * from STEP Tools, Inc. (www.steptools.com) 
 */

FILE_DESCRIPTION(
/* description */ ('', 'CAx-IF Rec.Pracs.---Representation and Presentation of Product Manufa
cturing Information (PMI)---4.0---2014-10-13'),
/* implementation_level */ '2;1');

FILE_NAME(
/* name */ 'Flat Washer M3.step',
/* time_stamp */ '2026-10-28T14:45:12+01:00',
/* author */ (''),
/* organization */ (''),
/* preprocessor_version */ 'ST-DEVELOPER v20.2',
/* originating_system */ 'Autodesk Translation Framework v15.17.0.0',
/* authorisation */ '');

FILE_SCHEMA (('AP242_MANAGED_MODEL_BASED_3D_ENGINEERING_MIM_LF { 1 0 10303 442 2 1 4 }'));
ENDSEC;

DATA;
#10=MECHANICAL_DESIGN_GEOMETRIC_PRESENTATION_REPRESENTATION('',(#261),#52164);
#208=TOROIDAL_SURFACE('',#9702,3.2,0.25);
#235=SHAPE_REPRESENTATION_RELATIONSHIP('SRR','None',#52214,#248);
#248=ADVANCED_BREP_SHAPE_REPRESENTATION('',(#274),#52154);
#261=STYLED_ITEM('',(#52325),#274);
#274=MANIFOLD_SOLID_BREP('Body1',#9121);
#297=FACE_BOUND('',#1273,.T.);
#298=FACE_BOUND('',#1276,.T.);
#436=PLANE('',#9695);
#437=PLANE('',#9700);
#726=FACE_OUTER_BOUND('',#1272,.T.);
#727=FACE_OUTER_BOUND('',#1274,.T.);
#728=FACE_OUTER_BOUND('',#1275,.T.);
#729=FACE_OUTER_BOUND('',#1277,.T.);
#1272=EDGE_LOOP('',(#6764));
#1273=EDGE_LOOP('',(#6765));
#1274=EDGE_LOOP('',(#6766,#6767,#6768,#6769));
#1275=EDGE_LOOP('',(#6770));
#1276=EDGE_LOOP('',(#6771));
#1277=EDGE_LOOP('',(#6772,#6773,#6774,#6775));
#1869=CIRCLE('',#9696,3.2);
#1870=CIRCLE('',#9697,1.6);
#1871=CIRCLE('',#9699,1.6);
#1872=CIRCLE('',#9701,3.2);
#1873=CIRCLE('',#9703,0.25);
#2673=LINE('',#25146,#3138);
#3138=VECTOR('',#11269,1.6);
#3767=VERTEX_POINT('',#25140);
#3768=VERTEX_POINT('',#25142);
#3769=VERTEX_POINT('',#25145);
#3770=VERTEX_POINT('',#25149);
#4828=EDGE_CURVE('',#3767,#3767,#1869,.T.);
#4829=EDGE_CURVE('',#3768,#3768,#1870,.T.);
#4830=EDGE_CURVE('',#3768,#3769,#2673,.T.);
#4831=EDGE_CURVE('',#3769,#3769,#1871,.T.);
#4832=EDGE_CURVE('',#3770,#3770,#1872,.T.);
#4833=EDGE_CURVE('',#3770,#3767,#1873,.T.);
#6764=ORIENTED_EDGE('',*,*,#4828,.T.);
#6765=ORIENTED_EDGE('',*,*,#4829,.F.);
#6766=ORIENTED_EDGE('',*,*,#4829,.T.);
#6767=ORIENTED_EDGE('',*,*,#4830,.T.);
#6768=ORIENTED_EDGE('',*,*,#4831,.F.);
#6769=ORIENTED_EDGE('',*,*,#4830,.F.);
#6770=ORIENTED_EDGE('',*,*,#4832,.T.);
#6771=ORIENTED_EDGE('',*,*,#4831,.T.);
#6772=ORIENTED_EDGE('',*,*,#4832,.F.);
#6773=ORIENTED_EDGE('',*,*,#4833,.T.);
#6774=ORIENTED_EDGE('',*,*,#4828,.F.);
#6775=ORIENTED_EDGE('',*,*,#4833,.F.);
#8491=CYLINDRICAL_SURFACE('',#9698,1.6);
#8789=ADVANCED_FACE('',(#726,#297),#436,.F.);
#8790=ADVANCED_FACE('',(#727),#8491,.F.);
#8791=ADVANCED_FACE('',(#728,#298),#437,.T.);
#8792=ADVANCED_FACE('',(#729),#208,.T.);
#9121=CLOSED_SHELL('',(#8789,#8790,#8791,#8792));
#9694=AXIS2_PLACEMENT_3D('',#25138,#11259,#11260);
#9695=AXIS2_PLACEMENT_3D('',#25139,#11261,#11262);
#9696=AXIS2_PLACEMENT_3D('',#25141,#11263,#11264);
#9697=AXIS2_PLACEMENT_3D('',#25143,#11265,#11266);
#9698=AXIS2_PLACEMENT_3D('',#25144,#11267,#11268);
#9699=AXIS2_PLACEMENT_3D('',#25147,#11270,#11271);
#9700=AXIS2_PLACEMENT_3D('',#25148,#11272,#11273);
#9701=AXIS2_PLACEMENT_3D('',#25150,#11274,#11275);
#9702=AXIS2_PLACEMENT_3D('',#25151,#11276,#11277);
#9703=AXIS2_PLACEMENT_3D('',#25152,#11278,#11279);
#11259=DIRECTION('axis',(0.,0.,1.));
#11260=DIRECTION('refdir',(1.,0.,0.));
#11261=DIRECTION('center_axis',(0.,1.,0.));
#11262=DIRECTION('ref_axis',(1.,0.,0.));
#11263=DIRECTION('center_axis',(0.,-1.,0.));
#11264=DIRECTION('ref_axis',(1.,0.,0.));
#11265=DIRECTION('center_axis',(0.,-1.,0.));
#11266=DIRECTION('ref_axis',(1.,0.,0.));
#11267=DIRECTION('center_axis',(0.,1.,0.));
#11268=DIRECTION('ref_axis',(1.,0.,0.));
#11269=DIRECTION('',(0.,1.,0.));
#11270=DIRECTION('center_axis',(0.,-1.,0.));
#11271=DIRECTION('ref_axis',(1.,0.,0.));
#11272=DIRECTION('center_axis',(0.,1.,0.));
#11273=DIRECTION('ref_axis',(1.,0.,0.));
#11274=DIRECTION('center_axis',(0.,1.,0.));
#11275=DIRECTION('ref_axis',(-1.,0.,0.));
#11276=DIRECTION('center_axis',(0.,1.,0.));
#11277=DIRECTION('ref_axis',(-0.999990518102908,0.,-0.00435473354849803));
#11278=DIRECTION('center_axis',(0.00435473354849791,0.,-0.999990518102908));
#11279=DIRECTION('ref_axis',(0.999990518102908,0.,0.00435473354849791));
#25138=CARTESIAN_POINT('',(0.,0.,0.));
#25139=CARTESIAN_POINT('Origin',(0.,0.,0.));
#25140=CARTESIAN_POINT('',(3.1999696579293,0.,0.0139351473551933));
#25141=CARTESIAN_POINT('Origin',(0.,0.,0.));
#25142=CARTESIAN_POINT('',(-1.6,0.,1.95943487863577E-16));
#25143=CARTESIAN_POINT('Origin',(0.,0.,0.));
#25144=CARTESIAN_POINT('Origin',(0.,0.,0.));
#25145=CARTESIAN_POINT('',(-1.6,0.5,1.95943487863577E-16));
#25146=CARTESIAN_POINT('',(-1.6,0.,1.95943487863577E-16));
#25147=CARTESIAN_POINT('Origin',(0.,0.5,0.));
#25148=CARTESIAN_POINT('Origin',(0.,0.5,0.));
#25149=CARTESIAN_POINT('',(3.1999696579293,0.5,0.0139351473551933));
#25150=CARTESIAN_POINT('Origin',(0.,0.5,0.));
#25151=CARTESIAN_POINT('Origin',(0.,0.25,0.));
#25152=CARTESIAN_POINT('Origin',(3.1999696579293,0.25,0.0139351473551933));
#52139=UNCERTAINTY_MEASURE_WITH_UNIT(LENGTH_MEASURE(0.01),#52165,
'DISTANCE_ACCURACY_VALUE',
'Maximum model space distance between geometric entities at asserted c
onnectivities');
#52149=UNCERTAINTY_MEASURE_WITH_UNIT(LENGTH_MEASURE(0.01),#52165,
'DISTANCE_ACCURACY_VALUE',
'Maximum model space distance between geometric entities at asserted c
onnectivities');
#52154=(
GEOMETRIC_REPRESENTATION_CONTEXT(3)
GLOBAL_UNCERTAINTY_ASSIGNED_CONTEXT((#52139))
GLOBAL_UNIT_ASSIGNED_CONTEXT((#52165,#52167,#52168))
REPRESENTATION_CONTEXT('','3D')
);
#52164=(
GEOMETRIC_REPRESENTATION_CONTEXT(3)
GLOBAL_UNCERTAINTY_ASSIGNED_CONTEXT((#52149))
GLOBAL_UNIT_ASSIGNED_CONTEXT((#52165,#52167,#52168))
REPRESENTATION_CONTEXT('','3D')
);
#52165=(
LENGTH_UNIT()
NAMED_UNIT(*)
SI_UNIT(.MILLI.,.METRE.)
);
#52167=(
NAMED_UNIT(*)
PLANE_ANGLE_UNIT()
SI_UNIT($,.RADIAN.)
);
#52168=(
NAMED_UNIT(*)
SI_UNIT($,.STERADIAN.)
SOLID_ANGLE_UNIT()
);
#52173=SHAPE_DEFINITION_REPRESENTATION(#52187,#52214);
#52187=PRODUCT_DEFINITION_SHAPE('',$,#52229);
#52214=SHAPE_REPRESENTATION('',(#9694),#52154);
#52224=PRODUCT_DEFINITION_CONTEXT('part definition',#52268,'design');
#52229=PRODUCT_DEFINITION('Flat Washer M3','Flat Washer M3',#52243,#52224);
#52243=PRODUCT_DEFINITION_FORMATION('',$,#52274);
#52268=APPLICATION_CONTEXT('Managed model based 3d engineering');
#52269=PRODUCT_CONTEXT('part definition',#52268,'mechanical');
#52274=PRODUCT('Flat Washer M3','Flat Washer M3','NOT SPECIFIED',(#52269));
#52319=COLOUR_RGB('Black',0.12,0.14,0.17);
#52320=FILL_AREA_STYLE_COLOUR('',#52319);
#52321=FILL_AREA_STYLE('',(#52320));
#52322=SURFACE_STYLE_FILL_AREA(#52321);
#52323=SURFACE_SIDE_STYLE('',(#52322));
#52324=SURFACE_STYLE_USAGE(.BOTH.,#52323);
#52325=PRESENTATION_STYLE_ASSIGNMENT((#52324));
ENDSEC;
END-ISO-10303-21;
